ISO-10303-21;
HEADER;
/* Generated by software containing ST-Developer
 * from STEP Tools, Inc. (www.steptools.com) 
 */

FILE_DESCRIPTION(
/* description */ ('PAT-112'),
/* implementation_level */ '2;1');

FILE_NAME(
/* name */ 'Cap Screw - M8x30.step',
/* time_stamp */ '2026-11-15T15:25:42-08:00',
/* author */ (''),
/* organization */ (''),
/* preprocessor_version */ 'ST-DEVELOPER v20.2',
/* originating_system */ 'Autodesk Translation Framework v15.17.0.0',
/* authorisation */ '');

FILE_SCHEMA (('AUTOMOTIVE_DESIGN { 1 0 10303 214 3 1 1 }'));
ENDSEC;

DATA;
#10=MECHANICAL_DESIGN_GEOMETRIC_PRESENTATION_REPRESENTATION('',(#111),#2277);
#11=CONICAL_SURFACE('',#1463,0.625,0.785398163397448);
#12=CONICAL_SURFACE('',#1467,0.635,0.785398163397449);
#13=CONICAL_SURFACE('',#1471,0.41,0.463647609000806);
#14=CONICAL_SURFACE('',#1475,0.36,0.785398163397448);
#15=ORIENTED_CLOSED_SHELL('',*,#1263,.F.);
#16=BREP_WITH_VOIDS('Body1',#1264,(#15));
#96=SHAPE_REPRESENTATION_RELATIONSHIP('SRR','None',#2325,#103);
#103=ADVANCED_BREP_SHAPE_REPRESENTATION('',(#16),#2275);
#111=STYLED_ITEM('',(#2371),#16);
#145=FACE_BOUND('',#369,.T.);
#184=PLANE('',#1453);
#185=PLANE('',#1454);
#186=PLANE('',#1455);
#187=PLANE('',#1456);
#188=PLANE('',#1457);
#189=PLANE('',#1458);
#190=PLANE('',#1459);
#191=PLANE('',#1460);
#192=PLANE('',#1461);
#193=PLANE('',#1469);
#194=PLANE('',#1477);
#254=FACE_OUTER_BOUND('',#356,.T.);
#255=FACE_OUTER_BOUND('',#357,.T.);
#256=FACE_OUTER_BOUND('',#358,.T.);
#257=FACE_OUTER_BOUND('',#359,.T.);
#258=FACE_OUTER_BOUND('',#360,.T.);
#259=FACE_OUTER_BOUND('',#361,.T.);
#260=FACE_OUTER_BOUND('',#362,.T.);
#261=FACE_OUTER_BOUND('',#363,.T.);
#262=FACE_OUTER_BOUND('',#364,.T.);
#263=FACE_OUTER_BOUND('',#365,.T.);
#264=FACE_OUTER_BOUND('',#366,.T.);
#265=FACE_OUTER_BOUND('',#367,.T.);
#266=FACE_OUTER_BOUND('',#368,.T.);
#267=FACE_OUTER_BOUND('',#370,.T.);
#268=FACE_OUTER_BOUND('',#371,.T.);
#269=FACE_OUTER_BOUND('',#372,.T.);
#270=FACE_OUTER_BOUND('',#373,.T.);
#356=EDGE_LOOP('',(#1090,#1091,#1092,#1093));
#357=EDGE_LOOP('',(#1094,#1095,#1096,#1097));
#358=EDGE_LOOP('',(#1098,#1099,#1100,#1101));
#359=EDGE_LOOP('',(#1102,#1103,#1104,#1105));
#360=EDGE_LOOP('',(#1106,#1107,#1108,#1109));
#361=EDGE_LOOP('',(#1110,#1111,#1112,#1113));
#362=EDGE_LOOP('',(#1114,#1115,#1116,#1117,#1118,#1119));
#363=EDGE_LOOP('',(#1120,#1121,#1122,#1123,#1124,#1125));
#364=EDGE_LOOP('',(#1126));
#365=EDGE_LOOP('',(#1127,#1128,#1129,#1130));
#366=EDGE_LOOP('',(#1131,#1132,#1133,#1134));
#367=EDGE_LOOP('',(#1135,#1136,#1137,#1138));
#368=EDGE_LOOP('',(#1139));
#369=EDGE_LOOP('',(#1140));
#370=EDGE_LOOP('',(#1141,#1142,#1143,#1144));
#371=EDGE_LOOP('',(#1145,#1146,#1147,#1148));
#372=EDGE_LOOP('',(#1149,#1150,#1151,#1152));
#373=EDGE_LOOP('',(#1153));
#447=LINE('',#2167,#542);
#448=LINE('',#2169,#543);
#449=LINE('',#2171,#544);
#450=LINE('',#2172,#545);
#451=LINE('',#2175,#546);
#452=LINE('',#2177,#547);
#453=LINE('',#2178,#548);
#454=LINE('',#2181,#549);
#455=LINE('',#2183,#550);
#456=LINE('',#2184,#551);
#457=LINE('',#2187,#552);
#458=LINE('',#2189,#553);
#459=LINE('',#2190,#554);
#460=LINE('',#2193,#555);
#461=LINE('',#2195,#556);
#462=LINE('',#2196,#557);
#463=LINE('',#2198,#558);
#464=LINE('',#2199,#559);
#465=LINE('',#2208,#560);
#466=LINE('',#2212,#561);
#467=LINE('',#2215,#562);
#468=LINE('',#2222,#563);
#469=LINE('',#2227,#564);
#470=LINE('',#2230,#565);
#542=VECTOR('',#1790,1.);
#543=VECTOR('',#1791,1.);
#544=VECTOR('',#1792,1.);
#545=VECTOR('',#1793,1.);
#546=VECTOR('',#1796,1.);
#547=VECTOR('',#1797,1.);
#548=VECTOR('',#1798,1.);
#549=VECTOR('',#1801,1.);
#550=VECTOR('',#1802,1.);
#551=VECTOR('',#1803,1.);
#552=VECTOR('',#1806,1.);
#553=VECTOR('',#1807,1.);
#554=VECTOR('',#1808,1.);
#555=VECTOR('',#1811,1.);
#556=VECTOR('',#1812,1.);
#557=VECTOR('',#1813,1.);
#558=VECTOR('',#1816,1.);
#559=VECTOR('',#1817,1.);
#560=VECTOR('',#1830,0.625);
#561=VECTOR('',#1835,0.65);
#562=VECTOR('',#1838,0.635);
#563=VECTOR('',#1847,0.41);
#564=VECTOR('',#1854,0.3933);
#565=VECTOR('',#1857,0.36);
#609=CIRCLE('',#1462,0.6);
#610=CIRCLE('',#1464,0.65);
#611=CIRCLE('',#1466,0.65);
#612=CIRCLE('',#1468,0.62);
#613=CIRCLE('',#1470,0.42);
#614=CIRCLE('',#1472,0.3933);
#615=CIRCLE('',#1474,0.3933);
#616=CIRCLE('',#1476,0.32);
#697=VERTEX_POINT('',#2165);
#698=VERTEX_POINT('',#2166);
#699=VERTEX_POINT('',#2168);
#700=VERTEX_POINT('',#2170);
#701=VERTEX_POINT('',#2174);
#702=VERTEX_POINT('',#2176);
#703=VERTEX_POINT('',#2180);
#704=VERTEX_POINT('',#2182);
#705=VERTEX_POINT('',#2186);
#706=VERTEX_POINT('',#2188);
#707=VERTEX_POINT('',#2192);
#708=VERTEX_POINT('',#2194);
#709=VERTEX_POINT('',#2203);
#710=VERTEX_POINT('',#2206);
#711=VERTEX_POINT('',#2210);
#712=VERTEX_POINT('',#2214);
#713=VERTEX_POINT('',#2218);
#714=VERTEX_POINT('',#2221);
#715=VERTEX_POINT('',#2225);
#716=VERTEX_POINT('',#2229);
#831=EDGE_CURVE('',#697,#698,#447,.T.);
#832=EDGE_CURVE('',#698,#699,#448,.T.);
#833=EDGE_CURVE('',#699,#700,#449,.T.);
#834=EDGE_CURVE('',#697,#700,#450,.T.);
#835=EDGE_CURVE('',#698,#701,#451,.T.);
#836=EDGE_CURVE('',#701,#702,#452,.T.);
#837=EDGE_CURVE('',#702,#699,#453,.T.);
#838=EDGE_CURVE('',#701,#703,#454,.T.);
#839=EDGE_CURVE('',#703,#704,#455,.T.);
#840=EDGE_CURVE('',#704,#702,#456,.T.);
#841=EDGE_CURVE('',#703,#705,#457,.T.);
#842=EDGE_CURVE('',#705,#706,#458,.T.);
#843=EDGE_CURVE('',#706,#704,#459,.T.);
#844=EDGE_CURVE('',#705,#707,#460,.T.);
#845=EDGE_CURVE('',#707,#708,#461,.T.);
#846=EDGE_CURVE('',#708,#706,#462,.T.);
#847=EDGE_CURVE('',#707,#697,#463,.T.);
#848=EDGE_CURVE('',#700,#708,#464,.T.);
#849=EDGE_CURVE('',#709,#709,#609,.T.);
#850=EDGE_CURVE('',#710,#710,#610,.T.);
#851=EDGE_CURVE('',#710,#709,#465,.T.);
#852=EDGE_CURVE('',#711,#711,#611,.T.);
#853=EDGE_CURVE('',#711,#710,#466,.T.);
#854=EDGE_CURVE('',#711,#712,#467,.T.);
#855=EDGE_CURVE('',#712,#712,#612,.T.);
#856=EDGE_CURVE('',#713,#713,#613,.T.);
#857=EDGE_CURVE('',#713,#714,#468,.T.);
#858=EDGE_CURVE('',#714,#714,#614,.F.);
#859=EDGE_CURVE('',#715,#715,#615,.F.);
#860=EDGE_CURVE('',#715,#714,#469,.T.);
#861=EDGE_CURVE('',#715,#716,#470,.T.);
#862=EDGE_CURVE('',#716,#716,#616,.T.);
#1090=ORIENTED_EDGE('',*,*,#831,.T.);
#1091=ORIENTED_EDGE('',*,*,#832,.T.);
#1092=ORIENTED_EDGE('',*,*,#833,.T.);
#1093=ORIENTED_EDGE('',*,*,#834,.F.);
#1094=ORIENTED_EDGE('',*,*,#835,.T.);
#1095=ORIENTED_EDGE('',*,*,#836,.T.);
#1096=ORIENTED_EDGE('',*,*,#837,.T.);
#1097=ORIENTED_EDGE('',*,*,#832,.F.);
#1098=ORIENTED_EDGE('',*,*,#838,.T.);
#1099=ORIENTED_EDGE('',*,*,#839,.T.);
#1100=ORIENTED_EDGE('',*,*,#840,.T.);
#1101=ORIENTED_EDGE('',*,*,#836,.F.);
#1102=ORIENTED_EDGE('',*,*,#841,.T.);
#1103=ORIENTED_EDGE('',*,*,#842,.T.);
#1104=ORIENTED_EDGE('',*,*,#843,.T.);
#1105=ORIENTED_EDGE('',*,*,#839,.F.);
#1106=ORIENTED_EDGE('',*,*,#844,.T.);
#1107=ORIENTED_EDGE('',*,*,#845,.T.);
#1108=ORIENTED_EDGE('',*,*,#846,.T.);
#1109=ORIENTED_EDGE('',*,*,#842,.F.);
#1110=ORIENTED_EDGE('',*,*,#847,.T.);
#1111=ORIENTED_EDGE('',*,*,#834,.T.);
#1112=ORIENTED_EDGE('',*,*,#848,.T.);
#1113=ORIENTED_EDGE('',*,*,#845,.F.);
#1114=ORIENTED_EDGE('',*,*,#847,.F.);
#1115=ORIENTED_EDGE('',*,*,#844,.F.);
#1116=ORIENTED_EDGE('',*,*,#841,.F.);
#1117=ORIENTED_EDGE('',*,*,#838,.F.);
#1118=ORIENTED_EDGE('',*,*,#835,.F.);
#1119=ORIENTED_EDGE('',*,*,#831,.F.);
#1120=ORIENTED_EDGE('',*,*,#848,.F.);
#1121=ORIENTED_EDGE('',*,*,#833,.F.);
#1122=ORIENTED_EDGE('',*,*,#837,.F.);
#1123=ORIENTED_EDGE('',*,*,#840,.F.);
#1124=ORIENTED_EDGE('',*,*,#843,.F.);
#1125=ORIENTED_EDGE('',*,*,#846,.F.);
#1126=ORIENTED_EDGE('',*,*,#849,.F.);
#1127=ORIENTED_EDGE('',*,*,#850,.F.);
#1128=ORIENTED_EDGE('',*,*,#851,.T.);
#1129=ORIENTED_EDGE('',*,*,#849,.T.);
#1130=ORIENTED_EDGE('',*,*,#851,.F.);
#1131=ORIENTED_EDGE('',*,*,#852,.F.);
#1132=ORIENTED_EDGE('',*,*,#853,.T.);
#1133=ORIENTED_EDGE('',*,*,#850,.T.);
#1134=ORIENTED_EDGE('',*,*,#853,.F.);
#1135=ORIENTED_EDGE('',*,*,#852,.T.);
#1136=ORIENTED_EDGE('',*,*,#854,.T.);
#1137=ORIENTED_EDGE('',*,*,#855,.F.);
#1138=ORIENTED_EDGE('',*,*,#854,.F.);
#1139=ORIENTED_EDGE('',*,*,#855,.T.);
#1140=ORIENTED_EDGE('',*,*,#856,.F.);
#1141=ORIENTED_EDGE('',*,*,#856,.T.);
#1142=ORIENTED_EDGE('',*,*,#857,.T.);
#1143=ORIENTED_EDGE('',*,*,#858,.F.);
#1144=ORIENTED_EDGE('',*,*,#857,.F.);
#1145=ORIENTED_EDGE('',*,*,#859,.F.);
#1146=ORIENTED_EDGE('',*,*,#860,.T.);
#1147=ORIENTED_EDGE('',*,*,#858,.T.);
#1148=ORIENTED_EDGE('',*,*,#860,.F.);
#1149=ORIENTED_EDGE('',*,*,#859,.T.);
#1150=ORIENTED_EDGE('',*,*,#861,.T.);
#1151=ORIENTED_EDGE('',*,*,#862,.F.);
#1152=ORIENTED_EDGE('',*,*,#861,.F.);
#1153=ORIENTED_EDGE('',*,*,#862,.T.);
#1177=CYLINDRICAL_SURFACE('',#1465,0.65);
#1178=CYLINDRICAL_SURFACE('',#1473,0.3933);
#1237=ADVANCED_FACE('',(#254),#184,.F.);
#1238=ADVANCED_FACE('',(#255),#185,.F.);
#1239=ADVANCED_FACE('',(#256),#186,.F.);
#1240=ADVANCED_FACE('',(#257),#187,.F.);
#1241=ADVANCED_FACE('',(#258),#188,.F.);
#1242=ADVANCED_FACE('',(#259),#189,.F.);
#1243=ADVANCED_FACE('',(#260),#190,.F.);
#1244=ADVANCED_FACE('',(#261),#191,.F.);
#1245=ADVANCED_FACE('',(#262),#192,.T.);
#1246=ADVANCED_FACE('',(#263),#11,.T.);
#1247=ADVANCED_FACE('',(#264),#1177,.T.);
#1248=ADVANCED_FACE('',(#265),#12,.T.);
#1249=ADVANCED_FACE('',(#266,#145),#193,.T.);
#1250=ADVANCED_FACE('',(#267),#13,.T.);
#1251=ADVANCED_FACE('',(#268),#1178,.T.);
#1252=ADVANCED_FACE('',(#269),#14,.T.);
#1253=ADVANCED_FACE('',(#270),#194,.T.);
#1263=CLOSED_SHELL('',(#1237,#1238,#1239,#1240,#1241,#1242,#1243,#1244));
#1264=CLOSED_SHELL('',(#1245,#1246,#1247,#1248,#1249,#1250,#1251,#1252,
#1253));
#1452=AXIS2_PLACEMENT_3D('',#2163,#1786,#1787);
#1453=AXIS2_PLACEMENT_3D('',#2164,#1788,#1789);
#1454=AXIS2_PLACEMENT_3D('',#2173,#1794,#1795);
#1455=AXIS2_PLACEMENT_3D('',#2179,#1799,#1800);
#1456=AXIS2_PLACEMENT_3D('',#2185,#1804,#1805);
#1457=AXIS2_PLACEMENT_3D('',#2191,#1809,#1810);
#1458=AXIS2_PLACEMENT_3D('',#2197,#1814,#1815);
#1459=AXIS2_PLACEMENT_3D('',#2200,#1818,#1819);
#1460=AXIS2_PLACEMENT_3D('',#2201,#1820,#1821);
#1461=AXIS2_PLACEMENT_3D('',#2202,#1822,#1823);
#1462=AXIS2_PLACEMENT_3D('',#2204,#1824,#1825);
#1463=AXIS2_PLACEMENT_3D('',#2205,#1826,#1827);
#1464=AXIS2_PLACEMENT_3D('',#2207,#1828,#1829);
#1465=AXIS2_PLACEMENT_3D('',#2209,#1831,#1832);
#1466=AXIS2_PLACEMENT_3D('',#2211,#1833,#1834);
#1467=AXIS2_PLACEMENT_3D('',#2213,#1836,#1837);
#1468=AXIS2_PLACEMENT_3D('',#2216,#1839,#1840);
#1469=AXIS2_PLACEMENT_3D('',#2217,#1841,#1842);
#1470=AXIS2_PLACEMENT_3D('',#2219,#1843,#1844);
#1471=AXIS2_PLACEMENT_3D('',#2220,#1845,#1846);
#1472=AXIS2_PLACEMENT_3D('',#2223,#1848,#1849);
#1473=AXIS2_PLACEMENT_3D('',#2224,#1850,#1851);
#1474=AXIS2_PLACEMENT_3D('',#2226,#1852,#1853);
#1475=AXIS2_PLACEMENT_3D('',#2228,#1855,#1856);
#1476=AXIS2_PLACEMENT_3D('',#2231,#1858,#1859);
#1477=AXIS2_PLACEMENT_3D('',#2232,#1860,#1861);
#1786=DIRECTION('axis',(0.,0.,1.));
#1787=DIRECTION('refdir',(1.,0.,0.));
#1788=DIRECTION('center_axis',(0.866025403784439,0.,-0.5));
#1789=DIRECTION('ref_axis',(0.5,0.,0.866025403784439));
#1790=DIRECTION('',(-0.5,0.,-0.866025403784439));
#1791=DIRECTION('',(0.,-1.,0.));
#1792=DIRECTION('',(0.5,0.,0.866025403784439));
#1793=DIRECTION('',(0.,-1.,0.));
#1794=DIRECTION('center_axis',(1.60246890531964E-16,0.,-1.));
#1795=DIRECTION('ref_axis',(1.,0.,1.60246890531964E-16));
#1796=DIRECTION('',(-1.,0.,-1.60246890531964E-16));
#1797=DIRECTION('',(0.,-1.,0.));
#1798=DIRECTION('',(1.,0.,1.60246890531964E-16));
#1799=DIRECTION('center_axis',(-0.866025403784439,0.,-0.5));
#1800=DIRECTION('ref_axis',(0.5,0.,-0.866025403784439));
#1801=DIRECTION('',(-0.5,0.,0.866025403784439));
#1802=DIRECTION('',(0.,-1.,0.));
#1803=DIRECTION('',(0.5,0.,-0.866025403784439));
#1804=DIRECTION('center_axis',(-0.866025403784439,0.,0.5));
#1805=DIRECTION('ref_axis',(-0.5,0.,-0.866025403784439));
#1806=DIRECTION('',(0.5,0.,0.866025403784439));
#1807=DIRECTION('',(0.,-1.,0.));
#1808=DIRECTION('',(-0.5,0.,-0.866025403784439));
#1809=DIRECTION('center_axis',(-1.60246890531964E-16,0.,1.));
#1810=DIRECTION('ref_axis',(-1.,0.,-1.60246890531964E-16));
#1811=DIRECTION('',(1.,0.,1.60246890531964E-16));
#1812=DIRECTION('',(0.,-1.,0.));
#1813=DIRECTION('',(-1.,0.,-1.60246890531964E-16));
#1814=DIRECTION('center_axis',(0.866025403784439,0.,0.5));
#1815=DIRECTION('ref_axis',(-0.5,0.,0.866025403784439));
#1816=DIRECTION('',(0.5,0.,-0.866025403784439));
#1817=DIRECTION('',(-0.5,0.,0.866025403784439));
#1818=DIRECTION('center_axis',(0.,1.,0.));
#1819=DIRECTION('ref_axis',(1.,0.,0.));
#1820=DIRECTION('center_axis',(0.,-1.,0.));
#1821=DIRECTION('ref_axis',(0.,0.,-1.));
#1822=DIRECTION('center_axis',(0.,1.,0.));
#1823=DIRECTION('ref_axis',(0.,0.,1.));
#1824=DIRECTION('center_axis',(0.,-1.,0.));
#1825=DIRECTION('ref_axis',(1.,0.,0.));
#1826=DIRECTION('center_axis',(0.,-1.,0.));
#1827=DIRECTION('ref_axis',(1.,0.,0.));
#1828=DIRECTION('center_axis',(0.,-1.,0.));
#1829=DIRECTION('ref_axis',(1.,0.,0.));
#1830=DIRECTION('',(0.707106781186547,0.707106781186548,8.65956056235493E-17));
#1831=DIRECTION('center_axis',(0.,-1.,0.));
#1832=DIRECTION('ref_axis',(1.,0.,0.));
#1833=DIRECTION('center_axis',(0.,-1.,0.));
#1834=DIRECTION('ref_axis',(1.,0.,0.));
#1835=DIRECTION('',(0.,1.,0.));
#1836=DIRECTION('center_axis',(0.,1.,0.));
#1837=DIRECTION('ref_axis',(1.,0.,0.));
#1838=DIRECTION('',(0.707106781186548,-0.707106781186547,-8.65956056235494E-17));
#1839=DIRECTION('center_axis',(0.,-1.,0.));
#1840=DIRECTION('ref_axis',(1.,0.,0.));
#1841=DIRECTION('center_axis',(0.,-1.,0.));
#1842=DIRECTION('ref_axis',(0.,0.,-1.));
#1843=DIRECTION('center_axis',(0.,-1.,0.));
#1844=DIRECTION('ref_axis',(1.,0.,0.));
#1845=DIRECTION('center_axis',(0.,1.,0.));
#1846=DIRECTION('ref_axis',(1.,0.,0.));
#1847=DIRECTION('',(0.447213595499958,-0.894427190999916,-5.47678698264203E-17));
#1848=DIRECTION('center_axis',(0.,1.,0.));
#1849=DIRECTION('ref_axis',(1.,0.,0.));
#1850=DIRECTION('center_axis',(0.,-1.,0.));
#1851=DIRECTION('ref_axis',(1.,0.,0.));
#1852=DIRECTION('center_axis',(0.,1.,0.));
#1853=DIRECTION('ref_axis',(1.,0.,0.));
#1854=DIRECTION('',(0.,1.,0.));
#1855=DIRECTION('center_axis',(0.,1.,0.));
#1856=DIRECTION('ref_axis',(1.,0.,0.));
#1857=DIRECTION('',(0.707106781186547,-0.707106781186548,-8.65956056235493E-17));
#1858=DIRECTION('center_axis',(0.,-1.,0.));
#1859=DIRECTION('ref_axis',(1.,0.,0.));
#1860=DIRECTION('center_axis',(0.,-1.,0.));
#1861=DIRECTION('ref_axis',(0.,0.,-1.));
#2163=CARTESIAN_POINT('',(0.,0.,0.));
#2164=CARTESIAN_POINT('Origin',(0.173205080756888,-0.8,-0.3));
#2165=CARTESIAN_POINT('',(0.346410161513775,-0.8,0.));
#2166=CARTESIAN_POINT('',(0.173205080756888,-0.8,-0.3));
#2167=CARTESIAN_POINT('',(0.346410161513775,-0.8,0.));
#2168=CARTESIAN_POINT('',(0.173205080756888,-1.28,-0.3));
#2169=CARTESIAN_POINT('',(0.173205080756888,-0.8,-0.3));
#2170=CARTESIAN_POINT('',(0.346410161513775,-1.28,0.));
#2171=CARTESIAN_POINT('',(0.346410161513775,-1.28,0.));
#2172=CARTESIAN_POINT('',(0.346410161513775,-0.8,0.));
#2173=CARTESIAN_POINT('Origin',(-0.173205080756888,-0.8,-0.3));
#2174=CARTESIAN_POINT('',(-0.173205080756888,-0.8,-0.3));
#2175=CARTESIAN_POINT('',(0.173205080756888,-0.8,-0.3));
#2176=CARTESIAN_POINT('',(-0.173205080756888,-1.28,-0.3));
#2177=CARTESIAN_POINT('',(-0.173205080756888,-0.8,-0.3));
#2178=CARTESIAN_POINT('',(0.173205080756888,-1.28,-0.3));
#2179=CARTESIAN_POINT('Origin',(-0.346410161513775,-0.8,-5.55111512312578E-17));
#2180=CARTESIAN_POINT('',(-0.346410161513775,-0.8,-4.24230095489963E-17));
#2181=CARTESIAN_POINT('',(-0.173205080756888,-0.8,-0.3));
#2182=CARTESIAN_POINT('',(-0.346410161513775,-1.28,-5.55111512312578E-17));
#2183=CARTESIAN_POINT('',(-0.346410161513775,-0.8,-4.24230095489963E-17));
#2184=CARTESIAN_POINT('',(-0.173205080756888,-1.28,-0.3));
#2185=CARTESIAN_POINT('Origin',(-0.173205080756888,-0.8,0.3));
#2186=CARTESIAN_POINT('',(-0.173205080756888,-0.8,0.3));
#2187=CARTESIAN_POINT('',(-0.346410161513775,-0.8,-4.24230095489963E-17));
#2188=CARTESIAN_POINT('',(-0.173205080756888,-1.28,0.3));
#2189=CARTESIAN_POINT('',(-0.173205080756888,-0.8,0.3));
#2190=CARTESIAN_POINT('',(-0.346410161513775,-1.28,-4.24230095489963E-17));
#2191=CARTESIAN_POINT('Origin',(0.173205080756888,-0.8,0.3));
#2192=CARTESIAN_POINT('',(0.173205080756888,-0.8,0.3));
#2193=CARTESIAN_POINT('',(-0.173205080756888,-0.8,0.3));
#2194=CARTESIAN_POINT('',(0.173205080756888,-1.28,0.3));
#2195=CARTESIAN_POINT('',(0.173205080756888,-0.8,0.3));
#2196=CARTESIAN_POINT('',(-0.173205080756888,-1.28,0.3));
#2197=CARTESIAN_POINT('Origin',(0.346410161513775,-0.8,0.));
#2198=CARTESIAN_POINT('',(0.173205080756888,-0.8,0.3));
#2199=CARTESIAN_POINT('',(0.173205080756888,-1.28,0.3));
#2200=CARTESIAN_POINT('Origin',(0.,-0.8,-5.55111512312578E-17));
#2201=CARTESIAN_POINT('Origin',(0.,-1.28,-5.55111512312578E-17));
#2202=CARTESIAN_POINT('Origin',(0.6,0.8,0.));
#2203=CARTESIAN_POINT('',(-0.6,0.8,-7.34788079488412E-17));
#2204=CARTESIAN_POINT('Origin',(0.,0.8,0.));
#2205=CARTESIAN_POINT('Origin',(0.,0.775,0.));
#2206=CARTESIAN_POINT('',(-0.65,0.75,-7.9602041944578E-17));
#2207=CARTESIAN_POINT('Origin',(0.,0.75,0.));
#2208=CARTESIAN_POINT('',(-0.625,0.775,-7.65404249467096E-17));
#2209=CARTESIAN_POINT('Origin',(0.,0.39,0.));
#2210=CARTESIAN_POINT('',(-0.65,0.0299999999999998,-7.9602041944578E-17));
#2211=CARTESIAN_POINT('Origin',(0.,0.0299999999999998,0.));
#2212=CARTESIAN_POINT('',(-0.65,0.39,-7.9602041944578E-17));
#2213=CARTESIAN_POINT('Origin',(0.,0.0150000000000001,0.));
#2214=CARTESIAN_POINT('',(-0.62,5.89805981832114E-17,-7.59281015471359E-17));
#2215=CARTESIAN_POINT('',(-0.635,0.0150000000000001,7.77650717458569E-17));
#2216=CARTESIAN_POINT('Origin',(0.,0.,0.));
#2217=CARTESIAN_POINT('Origin',(0.42,0.,0.));
#2218=CARTESIAN_POINT('',(-0.42,-3.46944695195361E-18,-5.14351655641888E-17));
#2219=CARTESIAN_POINT('Origin',(0.,0.,0.));
#2220=CARTESIAN_POINT('Origin',(0.,-0.02,0.));
#2221=CARTESIAN_POINT('',(-0.3933,-0.0534000000000001,4.81653586104654E-17));
#2222=CARTESIAN_POINT('',(-0.41,-0.02,5.02105187650415E-17));
#2223=CARTESIAN_POINT('Origin',(0.,-0.0534000000000001,0.));
#2224=CARTESIAN_POINT('Origin',(0.,-1.48,0.));
#2225=CARTESIAN_POINT('',(-0.3933,-2.9267,4.81653586104654E-17));
#2226=CARTESIAN_POINT('Origin',(0.,-2.9267,0.));
#2227=CARTESIAN_POINT('',(-0.3933,-1.48,-4.81653586104654E-17));
#2228=CARTESIAN_POINT('Origin',(0.,-2.96,0.));
#2229=CARTESIAN_POINT('',(-0.32,-3.,-3.91886975727153E-17));
#2230=CARTESIAN_POINT('',(-0.36,-2.96,4.40872847693047E-17));
#2231=CARTESIAN_POINT('Origin',(0.,-3.,0.));
#2232=CARTESIAN_POINT('Origin',(0.,-3.,0.));
#2265=UNCERTAINTY_MEASURE_WITH_UNIT(LENGTH_MEASURE(0.001),#2278,
'DISTANCE_ACCURACY_VALUE',
'Maximum model space distance between geometric entities at asserted c
onnectivities');
#2267=UNCERTAINTY_MEASURE_WITH_UNIT(LENGTH_MEASURE(0.001),#2278,
'DISTANCE_ACCURACY_VALUE',
'Maximum model space distance between geometric entities at asserted c
onnectivities');
#2275=(
GEOMETRIC_REPRESENTATION_CONTEXT(3)
GLOBAL_UNCERTAINTY_ASSIGNED_CONTEXT((#2265))
GLOBAL_UNIT_ASSIGNED_CONTEXT((#2278,#2280,#2281))
REPRESENTATION_CONTEXT('','3D')
);
#2277=(
GEOMETRIC_REPRESENTATION_CONTEXT(3)
GLOBAL_UNCERTAINTY_ASSIGNED_CONTEXT((#2267))
GLOBAL_UNIT_ASSIGNED_CONTEXT((#2278,#2280,#2281))
REPRESENTATION_CONTEXT('','3D')
);
#2278=(
LENGTH_UNIT()
NAMED_UNIT(*)
SI_UNIT(.CENTI.,.METRE.)
);
#2280=(
NAMED_UNIT(*)
PLANE_ANGLE_UNIT()
SI_UNIT($,.RADIAN.)
);
#2281=(
NAMED_UNIT(*)
SI_UNIT($,.STERADIAN.)
SOLID_ANGLE_UNIT()
);
#2289=SHAPE_DEFINITION_REPRESENTATION(#2300,#2325);
#2300=PRODUCT_DEFINITION_SHAPE('',$,#2335);
#2325=SHAPE_REPRESENTATION('',(#1452),#2275);
#2327=PRODUCT_DEFINITION_CONTEXT('part definition',#2356,'design');
#2335=PRODUCT_DEFINITION('Cap Screw - M8x30','Cap Screw - M8x30',#2344,
#2327);
#2344=PRODUCT_DEFINITION_FORMATION('',$,#2365);
#2356=APPLICATION_CONTEXT(
'Core Data for Automotive Mechanical Design Process');
#2357=PRODUCT_CONTEXT('part definition',#2356,'mechanical');
#2365=PRODUCT('Cap Screw - M8x30','Cap Screw - M8x30',
'Cap Screw - M8x30',(#2357));
#2371=PRESENTATION_STYLE_ASSIGNMENT((#2376));
#2376=SURFACE_STYLE_USAGE(.BOTH.,#2381);
#2381=SURFACE_SIDE_STYLE('',(#2386));
#2386=SURFACE_STYLE_FILL_AREA(#2391);
#2391=FILL_AREA_STYLE('Opaque(31,36,43)',(#2396));
#2396=FILL_AREA_STYLE_COLOUR('Opaque(31,36,43)',#2401);
#2401=COLOUR_RGB('Opaque(31,36,43)',0.12156862745098,0.141176470588235,
0.168627450980392);
ENDSEC;
END-ISO-10303-21;
